ISO-10303-21;
HEADER;
/* Generated by software containing ST-Developer
 * from STEP Tools, Inc. (www.steptools.com) 
 */

FILE_DESCRIPTION(
/* description */ (''),
/* implementation_level */ '2;1');

FILE_NAME(
/* name */ 'Spring_03.step',
/* time_stamp */ '2026-10-23T17:00:58+06:00',
/* author */ (''),
/* organization */ (''),
/* preprocessor_version */ 'ST-DEVELOPER v20.2',
/* originating_system */ 'Autodesk Translation Framework v15.15.0.0',
/* authorisation */ '');

FILE_SCHEMA (('AUTOMOTIVE_DESIGN { 1 0 10303 214 3 1 1 }'));
ENDSEC;

DATA;
#10=MECHANICAL_DESIGN_GEOMETRIC_PRESENTATION_REPRESENTATION('',(#116),#11385);
#72=B_SPLINE_SURFACE_WITH_KNOTS('',3,3,((#10857,#10858,#10859,#10860,#10861,
#10862,#10863,#10864,#10865,#10866,#10867,#10868,#10869,#10870,#10871,#10872,
#10873,#10874,#10875,#10876,#10877,#10878,#10879,#10880,#10881,#10882,#10883,
#10884,#10885,#10886,#10887,#10888,#10889,#10890,#10891,#10892,#10893),
(#10894,#10895,#10896,#10897,#10898,#10899,#10900,#10901,#10902,#10903,
#10904,#10905,#10906,#10907,#10908,#10909,#10910,#10911,#10912,#10913,#10914,
#10915,#10916,#10917,#10918,#10919,#10920,#10921,#10922,#10923,#10924,#10925,
#10926,#10927,#10928,#10929,#10930),(#10931,#10932,#10933,#10934,#10935,
#10936,#10937,#10938,#10939,#10940,#10941,#10942,#10943,#10944,#10945,#10946,
#10947,#10948,#10949,#10950,#10951,#10952,#10953,#10954,#10955,#10956,#10957,
#10958,#10959,#10960,#10961,#10962,#10963,#10964,#10965,#10966,#10967),
(#10968,#10969,#10970,#10971,#10972,#10973,#10974,#10975,#10976,#10977,
#10978,#10979,#10980,#10981,#10982,#10983,#10984,#10985,#10986,#10987,#10988,
#10989,#10990,#10991,#10992,#10993,#10994,#10995,#10996,#10997,#10998,#10999,
#11000,#11001,#11002,#11003,#11004),(#11005,#11006,#11007,#11008,#11009,
#11010,#11011,#11012,#11013,#11014,#11015,#11016,#11017,#11018,#11019,#11020,
#11021,#11022,#11023,#11024,#11025,#11026,#11027,#11028,#11029,#11030,#11031,
#11032,#11033,#11034,#11035,#11036,#11037,#11038,#11039,#11040,#11041),
(#11042,#11043,#11044,#11045,#11046,#11047,#11048,#11049,#11050,#11051,
#11052,#11053,#11054,#11055,#11056,#11057,#11058,#11059,#11060,#11061,#11062,
#11063,#11064,#11065,#11066,#11067,#11068,#11069,#11070,#11071,#11072,#11073,
#11074,#11075,#11076,#11077,#11078),(#11079,#11080,#11081,#11082,#11083,
#11084,#11085,#11086,#11087,#11088,#11089,#11090,#11091,#11092,#11093,#11094,
#11095,#11096,#11097,#11098,#11099,#11100,#11101,#11102,#11103,#11104,#11105,
#11106,#11107,#11108,#11109,#11110,#11111,#11112,#11113,#11114,#11115),
(#11116,#11117,#11118,#11119,#11120,#11121,#11122,#11123,#11124,#11125,
#11126,#11127,#11128,#11129,#11130,#11131,#11132,#11133,#11134,#11135,#11136,
#11137,#11138,#11139,#11140,#11141,#11142,#11143,#11144,#11145,#11146,#11147,
#11148,#11149,#11150,#11151,#11152),(#11153,#11154,#11155,#11156,#11157,
#11158,#11159,#11160,#11161,#11162,#11163,#11164,#11165,#11166,#11167,#11168,
#11169,#11170,#11171,#11172,#11173,#11174,#11175,#11176,#11177,#11178,#11179,
#11180,#11181,#11182,#11183,#11184,#11185,#11186,#11187,#11188,#11189),
(#11190,#11191,#11192,#11193,#11194,#11195,#11196,#11197,#11198,#11199,
#11200,#11201,#11202,#11203,#11204,#11205,#11206,#11207,#11208,#11209,#11210,
#11211,#11212,#11213,#11214,#11215,#11216,#11217,#11218,#11219,#11220,#11221,
#11222,#11223,#11224,#11225,#11226)),.UNSPECIFIED.,.T.,.F.,.F.,(4,1,1,1,
1,1,1,4),(4,1,1,1,1,1,1,1,1,1,1,1,1,1,1,1,1,1,1,1,1,1,1,1,1,1,1,1,1,1,1,
1,1,1,4),(-3.14159265358979,-2.24399475256414,-1.34639685153848,-0.448798950512828,
0.448798950512828,1.34639685153848,2.24399475256414,3.14159265358979),(0.,
0.490873852123405,0.98174770424681,1.96349540849362,2.94524311274043,3.92699081698724,
4.90873852123405,5.89048622548086,6.87223392972767,7.85398163397448,8.83572933822129,
9.8174770424681,10.7992247467149,11.7809724509617,12.7627201552085,13.7444678594553,
14.7262155637022,15.707963267949,16.6897109721958,17.6714586764426,18.6532063806894,
19.6349540849362,20.616701789183,21.5984494934298,22.5801971976766,23.5619449019234,
24.5436926061703,25.5254403104171,26.5071880146639,27.4889357189107,28.4706834231575,
29.4524311274043,30.4341788316511,30.9250526837745,31.4159265358979),
 .UNSPECIFIED.);
#78=TOROIDAL_SURFACE('',#6060,1.,0.25);
#90=SHAPE_REPRESENTATION_RELATIONSHIP('SRR','None',#11442,#103);
#103=ADVANCED_BREP_SHAPE_REPRESENTATION('',(#129),#11382);
#116=STYLED_ITEM('',(#11567),#129);
#129=MANIFOLD_SOLID_BREP('Spring_03',#5352);
#170=FACE_BOUND('',#1274,.T.);
#181=B_SPLINE_CURVE_WITH_KNOTS('',3,(#10813,#10814,#10815,#10816,#10817,
#10818,#10819,#10820,#10821,#10822,#10823,#10824,#10825,#10826,#10827,#10828,
#10829,#10830,#10831,#10832,#10833,#10834,#10835,#10836,#10837,#10838,#10839,
#10840,#10841,#10842,#10843,#10844,#10845,#10846,#10847,#10848,#10849,#10850,
#10851,#10852,#10853,#10854,#10855,#10856),.UNSPECIFIED.,.F.,.F.,(4,2,2,
2,2,2,2,2,2,2,2,2,2,2,2,2,2,2,2,2,2,4),(-0.181685657499379,-0.180553745361431,
-0.170622434730818,-0.170447684206912,-0.167737370927117,-0.166612489538818,
-0.16575101153334,-0.16478662015514,-0.16342132279605,-0.160072321773434,
-0.151029759575816,-0.145020173168477,-0.126301129887337,-0.111561605759352,
-0.101015311157688,-0.0928919097586381,-0.0856896815461206,-0.0776947291824182,
-0.0660486167614411,-0.0443043011100664,0.,0.000811103137473634),
 .UNSPECIFIED.);
#182=B_SPLINE_CURVE_WITH_KNOTS('',3,(#11228,#11229,#11230,#11231,#11232,
#11233,#11234,#11235,#11236,#11237,#11238,#11239,#11240,#11241,#11242,#11243,
#11244,#11245,#11246,#11247,#11248,#11249,#11250,#11251,#11252,#11253,#11254,
#11255,#11256,#11257,#11258,#11259,#11260,#11261,#11262,#11263,#11264),
 .UNSPECIFIED.,.F.,.F.,(4,1,1,1,1,1,1,1,1,1,1,1,1,1,1,1,1,1,1,1,1,1,1,1,
1,1,1,1,1,1,1,1,1,1,4),(0.,0.490873852123405,0.98174770424681,1.96349540849362,
2.94524311274043,3.92699081698724,4.90873852123405,5.89048622548086,6.87223392972767,
7.85398163397448,8.83572933822129,9.8174770424681,10.7992247467149,11.7809724509617,
12.7627201552085,13.7444678594553,14.7262155637022,15.707963267949,16.6897109721958,
17.6714586764426,18.6532063806894,19.6349540849362,20.616701789183,21.5984494934298,
22.5801971976766,23.5619449019234,24.5436926061703,25.5254403104171,26.5071880146639,
27.4889357189107,28.4706834231575,29.4524311274043,30.4341788316511,30.9250526837745,
31.4159265358979),.UNSPECIFIED.);
#520=CIRCLE('',#6061,0.25);
#521=CIRCLE('',#6062,0.75);
#522=CIRCLE('',#6063,0.25);
#523=CIRCLE('',#6064,0.25);
#909=FACE_OUTER_BOUND('',#1273,.T.);
#910=FACE_OUTER_BOUND('',#1275,.T.);
#911=FACE_OUTER_BOUND('',#1276,.T.);
#1273=EDGE_LOOP('',(#4786,#4787,#4788,#4789));
#1274=EDGE_LOOP('',(#4790,#4791));
#1275=EDGE_LOOP('',(#4792,#4793,#4794,#4795,#4796));
#1276=EDGE_LOOP('',(#4797));
#2638=VERTEX_POINT('',#10807);
#2639=VERTEX_POINT('',#10810);
#2640=VERTEX_POINT('',#10811);
#2641=VERTEX_POINT('',#11227);
#3358=EDGE_CURVE('',#2638,#2638,#520,.T.);
#3359=EDGE_CURVE('',#2638,#2638,#521,.T.);
#3360=EDGE_CURVE('',#2639,#2640,#522,.T.);
#3361=EDGE_CURVE('',#2639,#2640,#181,.T.);
#3362=EDGE_CURVE('',#2640,#2641,#182,.T.);
#3363=EDGE_CURVE('',#2641,#2641,#523,.T.);
#4786=ORIENTED_EDGE('',*,*,#3358,.T.);
#4787=ORIENTED_EDGE('',*,*,#3359,.T.);
#4788=ORIENTED_EDGE('',*,*,#3358,.F.);
#4789=ORIENTED_EDGE('',*,*,#3359,.F.);
#4790=ORIENTED_EDGE('',*,*,#3360,.F.);
#4791=ORIENTED_EDGE('',*,*,#3361,.T.);
#4792=ORIENTED_EDGE('',*,*,#3361,.F.);
#4793=ORIENTED_EDGE('',*,*,#3360,.T.);
#4794=ORIENTED_EDGE('',*,*,#3362,.T.);
#4795=ORIENTED_EDGE('',*,*,#3363,.T.);
#4796=ORIENTED_EDGE('',*,*,#3362,.F.);
#4797=ORIENTED_EDGE('',*,*,#3363,.F.);
#5004=PLANE('',#6065);
#5321=ADVANCED_FACE('',(#909,#170),#78,.T.);
#5322=ADVANCED_FACE('',(#910),#72,.F.);
#5323=ADVANCED_FACE('',(#911),#5004,.F.);
#5352=CLOSED_SHELL('',(#5321,#5322,#5323));
#6059=AXIS2_PLACEMENT_3D('',#10805,#7669,#7670);
#6060=AXIS2_PLACEMENT_3D('',#10806,#7671,#7672);
#6061=AXIS2_PLACEMENT_3D('',#10808,#7673,#7674);
#6062=AXIS2_PLACEMENT_3D('',#10809,#7675,#7676);
#6063=AXIS2_PLACEMENT_3D('',#10812,#7677,#7678);
#6064=AXIS2_PLACEMENT_3D('',#11265,#7679,#7680);
#6065=AXIS2_PLACEMENT_3D('',#11266,#7681,#7682);
#7669=DIRECTION('axis',(0.,0.,1.));
#7670=DIRECTION('refdir',(1.,0.,0.));
#7671=DIRECTION('center_axis',(2.22044604925031E-16,-1.,-1.22464679914735E-16));
#7672=DIRECTION('ref_axis',(0.,0.,-1.));
#7673=DIRECTION('center_axis',(-1.,-2.22044604925031E-16,0.));
#7674=DIRECTION('ref_axis',(0.,0.,1.));
#7675=DIRECTION('center_axis',(2.22044604925031E-16,-1.,-1.22464679914735E-16));
#7676=DIRECTION('ref_axis',(-2.71926214689378E-32,1.22464679914735E-16,
-1.));
#7677=DIRECTION('center_axis',(-1.,-2.22044604925031E-16,-2.71926214689378E-32));
#7678=DIRECTION('ref_axis',(-2.22044604925031E-16,1.,1.22464679914735E-16));
#7679=DIRECTION('center_axis',(1.,-1.00260219422232E-15,-1.22783356797248E-31));
#7680=DIRECTION('ref_axis',(1.00260219422232E-15,1.,1.22464679914735E-16));
#7681=DIRECTION('center_axis',(1.,-1.00260219422232E-15,-1.22783356797248E-31));
#7682=DIRECTION('ref_axis',(0.,1.22464679914735E-16,-1.));
#10805=CARTESIAN_POINT('',(0.,0.,0.));
#10806=CARTESIAN_POINT('Origin',(-18.7359120418715,26.3504782148047,17.6));
#10807=CARTESIAN_POINT('',(-18.7359120418715,26.3504782148047,18.35));
#10808=CARTESIAN_POINT('Origin',(-18.7359120418715,26.3504782148047,18.6));
#10809=CARTESIAN_POINT('Origin',(-18.7359120418715,26.3504782148047,17.6));
#10810=CARTESIAN_POINT('',(-18.7359120418715,26.6004782148047,16.6));
#10811=CARTESIAN_POINT('',(-18.7359120418715,26.1004782148047,16.6));
#10812=CARTESIAN_POINT('Origin',(-18.7359120418715,26.3504782148047,16.6));
#10813=CARTESIAN_POINT('Ctrl Pts',(-18.7359120418715,26.6004782148047,16.6));
#10814=CARTESIAN_POINT('Ctrl Pts',(-18.7402193353539,26.6004782148047,16.5977092724426));
#10815=CARTESIAN_POINT('Ctrl Pts',(-18.7445589464746,26.6004467587024,16.5954788663774));
#10816=CARTESIAN_POINT('Ctrl Pts',(-18.7872540124717,26.5998563522904,16.5742560748851));
#10817=CARTESIAN_POINT('Ctrl Pts',(-18.8283064246552,26.5971771315259,16.559542959919));
#10818=CARTESIAN_POINT('Ctrl Pts',(-18.8701108612612,26.5930900009076,16.5481972195909));
#10819=CARTESIAN_POINT('Ctrl Pts',(-18.8708339684841,26.5930188703742,16.5480020646239));
#10820=CARTESIAN_POINT('Ctrl Pts',(-18.8827759229911,26.5918370097103,16.544797109728));
#10821=CARTESIAN_POINT('Ctrl Pts',(-18.894063293504,26.590615824153,16.5420298581508));
#10822=CARTESIAN_POINT('Ctrl Pts',(-18.910070277255,26.5887362807543,16.5384418503857));
#10823=CARTESIAN_POINT('Ctrl Pts',(-18.9147727349573,26.5881661562854,16.5374286265409));
#10824=CARTESIAN_POINT('Ctrl Pts',(-18.9230847074372,26.5871263380585,16.5357072275207));
#10825=CARTESIAN_POINT('Ctrl Pts',(-18.9266932353496,26.5866642710644,16.5349829852478));
#10826=CARTESIAN_POINT('Ctrl Pts',(-18.9343464784642,26.585661455081,16.5334946079531));
#10827=CARTESIAN_POINT('Ctrl Pts',(-18.9383928290144,26.5851177664648,16.5327358435474));
#10828=CARTESIAN_POINT('Ctrl Pts',(-18.9481733797635,26.5837704893605,16.5309679692519));
#10829=CARTESIAN_POINT('Ctrl Pts',(-18.9539124540547,26.5829524731398,16.5299854641958));
#10830=CARTESIAN_POINT('Ctrl Pts',(-18.9737387918633,26.5800291593595,16.5267739133408));
#10831=CARTESIAN_POINT('Ctrl Pts',(-18.9878669666236,26.577776425181,16.5248034466825));
#10832=CARTESIAN_POINT('Ctrl Pts',(-19.0400872187947,26.568769854808,16.5186110231589));
#10833=CARTESIAN_POINT('Ctrl Pts',(-19.0785053382042,26.5608013780416,16.5162061142361));
#10834=CARTESIAN_POINT('Ctrl Pts',(-19.1413563804704,26.5448431161272,16.5154725363415));
#10835=CARTESIAN_POINT('Ctrl Pts',(-19.1663341463412,26.5377137973801,16.5160451884648));
#10836=CARTESIAN_POINT('Ctrl Pts',(-19.2675067236831,26.5048705240401,16.5219235534991));
#10837=CARTESIAN_POINT('Ctrl Pts',(-19.3339527175624,26.4736908333921,16.5341985199053));
#10838=CARTESIAN_POINT('Ctrl Pts',(-19.4275973319121,26.408664050569,16.5639151059098));
#10839=CARTESIAN_POINT('Ctrl Pts',(-19.4584745098273,26.3779628401158,16.5791986989673));
#10840=CARTESIAN_POINT('Ctrl Pts',(-19.493043062557,26.3250017138209,16.605627659773));
#10841=CARTESIAN_POINT('Ctrl Pts',(-19.5019011653722,26.3029596082007,16.6166575639151));
#10842=CARTESIAN_POINT('Ctrl Pts',(-19.5077448592175,26.2652062478922,16.6350648852536));
#10843=CARTESIAN_POINT('Ctrl Pts',(-19.5070741798815,26.2486012355754,16.6429988757827));
#10844=CARTESIAN_POINT('Ctrl Pts',(-19.498268450351,26.2180039204305,16.6569651923278));
#10845=CARTESIAN_POINT('Ctrl Pts',(-19.4911945436197,26.2046479601392,16.6627780404676));
#10846=CARTESIAN_POINT('Ctrl Pts',(-19.4706730422176,26.17894609994,16.6732083185761));
#10847=CARTESIAN_POINT('Ctrl Pts',(-19.4571316130369,26.1675135294197,16.677362768157));
#10848=CARTESIAN_POINT('Ctrl Pts',(-19.4199753453774,26.1438724951594,16.6848437491615));
#10849=CARTESIAN_POINT('Ctrl Pts',(-19.3946921404572,26.1337519058654,16.686910649375));
#10850=CARTESIAN_POINT('Ctrl Pts',(-19.3217072854985,26.1124320719796,16.6888104810606));
#10851=CARTESIAN_POINT('Ctrl Pts',(-19.2671883817412,26.1060347853434,16.6853604690573));
#10852=CARTESIAN_POINT('Ctrl Pts',(-19.0981182229277,26.0969290280957,16.6690502405298));
#10853=CARTESIAN_POINT('Ctrl Pts',(-18.8857203861473,26.1008383327785,16.6427595546923));
#10854=CARTESIAN_POINT('Ctrl Pts',(-18.741103632581,26.1004816814786,16.6015112866721));
#10855=CARTESIAN_POINT('Ctrl Pts',(-18.7385065750259,26.1004782148047,16.6007604391535));
#10856=CARTESIAN_POINT('Ctrl Pts',(-18.7359120418715,26.1004782148047,16.6));
#10857=CARTESIAN_POINT('Ctrl Pts',(-18.7359120418715,26.1004782148047,16.6));
#10858=CARTESIAN_POINT('Ctrl Pts',(-18.899536659246,26.1004782148047,16.553125));
#10859=CARTESIAN_POINT('Ctrl Pts',(-19.2254952210856,26.0179991230989,16.459375));
#10860=CARTESIAN_POINT('Ctrl Pts',(-19.7300373474021,25.5673218790664,16.271875));
#10861=CARTESIAN_POINT('Ctrl Pts',(-19.8229633788124,24.6519659680192,16.0375));
#10862=CARTESIAN_POINT('Ctrl Pts',(-18.9648841528132,23.9466522306267,15.75625));
#10863=CARTESIAN_POINT('Ctrl Pts',(-17.9047456459512,24.2694552701876,15.475));
#10864=CARTESIAN_POINT('Ctrl Pts',(-17.5826797074142,25.3296825136249,15.19375));
#10865=CARTESIAN_POINT('Ctrl Pts',(-18.2860294065758,26.1867906898977,14.9125));
#10866=CARTESIAN_POINT('Ctrl Pts',(-19.389086573694,26.0780174976981,14.63125));
#10867=CARTESIAN_POINT('Ctrl Pts',(-19.9116498391532,25.1004985660911,14.35));
#10868=CARTESIAN_POINT('Ctrl Pts',(-19.3891045896494,24.1228877031823,14.06875));
#10869=CARTESIAN_POINT('Ctrl Pts',(-18.2859840561,24.0142539916667,13.7875));
#10870=CARTESIAN_POINT('Ctrl Pts',(-17.582775853732,24.8711029879984,13.50625));
#10871=CARTESIAN_POINT('Ctrl Pts',(-17.9045489079489,25.9318432698064,13.225));
#10872=CARTESIAN_POINT('Ctrl Pts',(-18.9652844651045,26.2536123707356,12.94375));
#10873=CARTESIAN_POINT('Ctrl Pts',(-19.8221414011456,25.5504093950162,12.6625));
#10874=CARTESIAN_POINT('Ctrl Pts',(-19.7134924282747,24.4472796581219,12.38125));
#10875=CARTESIAN_POINT('Ctrl Pts',(-18.7359120418715,23.9247523488297,12.1));
#10876=CARTESIAN_POINT('Ctrl Pts',(-17.7583316554683,24.4472796581219,11.81875));
#10877=CARTESIAN_POINT('Ctrl Pts',(-17.6496826825974,25.5504093950162,11.5375));
#10878=CARTESIAN_POINT('Ctrl Pts',(-18.5065396186384,26.2536123707357,11.25625));
#10879=CARTESIAN_POINT('Ctrl Pts',(-19.567275175794,25.9318432698063,10.975));
#10880=CARTESIAN_POINT('Ctrl Pts',(-19.8890482300109,24.8711029879984,10.69375));
#10881=CARTESIAN_POINT('Ctrl Pts',(-19.185840027643,24.0142539916666,10.4125));
#10882=CARTESIAN_POINT('Ctrl Pts',(-18.0827194940936,24.1228877031824,10.13125));
#10883=CARTESIAN_POINT('Ctrl Pts',(-17.5601742445898,25.1004985660911,9.85));
#10884=CARTESIAN_POINT('Ctrl Pts',(-18.082737510049,26.0780174976981,9.56875));
#10885=CARTESIAN_POINT('Ctrl Pts',(-19.1857946771672,26.1867906898977,9.2875));
#10886=CARTESIAN_POINT('Ctrl Pts',(-19.8891443763288,25.329682513625,9.00625));
#10887=CARTESIAN_POINT('Ctrl Pts',(-19.5670784377918,24.2694552701875,8.725));
#10888=CARTESIAN_POINT('Ctrl Pts',(-18.5069399309298,23.9466522306267,8.44375));
#10889=CARTESIAN_POINT('Ctrl Pts',(-17.6488607049306,24.6519659680192,8.16250000000001));
#10890=CARTESIAN_POINT('Ctrl Pts',(-17.7417867363409,25.5673218790663,7.928125));
#10891=CARTESIAN_POINT('Ctrl Pts',(-18.2463288626574,26.0179991230989,7.740625));
#10892=CARTESIAN_POINT('Ctrl Pts',(-18.572287424497,26.1004782148047,7.646875));
#10893=CARTESIAN_POINT('Ctrl Pts',(-18.7359120418715,26.1004782148047,7.6));
#10894=CARTESIAN_POINT('Ctrl Pts',(-18.7359120418715,26.1004782148047,16.5252001749145));
#10895=CARTESIAN_POINT('Ctrl Pts',(-18.8994338407553,26.1004782148047,16.4783251749145));
#10896=CARTESIAN_POINT('Ctrl Pts',(-19.2255030930883,26.0179660342054,16.3845751749145));
#10897=CARTESIAN_POINT('Ctrl Pts',(-19.729867953292,25.5673943129456,16.1970751749145));
#10898=CARTESIAN_POINT('Ctrl Pts',(-19.8229695302986,24.6519424250744,15.9627001749145));
#10899=CARTESIAN_POINT('Ctrl Pts',(-18.9648436629017,23.9467315923973,15.6814501749145));
#10900=CARTESIAN_POINT('Ctrl Pts',(-17.9048011394298,24.2694854426487,15.4002001749145));
#10901=CARTESIAN_POINT('Ctrl Pts',(-17.5827296870337,25.3296765835496,15.1189501749145));
#10902=CARTESIAN_POINT('Ctrl Pts',(-18.2860551788254,26.1867342513203,14.8377001749145));
#10903=CARTESIAN_POINT('Ctrl Pts',(-19.3890525137468,26.0779704411713,14.5564501749145));
#10904=CARTESIAN_POINT('Ctrl Pts',(-19.9115925078101,25.1004979111444,14.2752001749145));
#10905=CARTESIAN_POINT('Ctrl Pts',(-19.3890718388655,24.1229364083568,13.9939501749145));
#10906=CARTESIAN_POINT('Ctrl Pts',(-18.2860065328672,24.0143075901023,13.7127001749145));
#10907=CARTESIAN_POINT('Ctrl Pts',(-17.582832820097,24.8711144190662,13.4314501749145));
#10908=CARTESIAN_POINT('Ctrl Pts',(-17.9045901039069,25.9318020855622,13.1502001749145));
#10909=CARTESIAN_POINT('Ctrl Pts',(-18.9652730883107,26.2535553206106,12.8689501749145));
#10910=CARTESIAN_POINT('Ctrl Pts',(-19.8220876543766,25.550387117378,12.5877001749145));
#10911=CARTESIAN_POINT('Ctrl Pts',(-19.7134440422139,24.4473119914142,12.3064501749145));
#10912=CARTESIAN_POINT('Ctrl Pts',(-18.7359120418715,23.9248105319629,12.0252001749145));
#10913=CARTESIAN_POINT('Ctrl Pts',(-17.7583800415291,24.4473119914142,11.7439501749145));
#10914=CARTESIAN_POINT('Ctrl Pts',(-17.6497364293663,25.550387117378,11.4627001749145));
#10915=CARTESIAN_POINT('Ctrl Pts',(-18.5065509954323,26.2535553206107,11.1814501749145));
#10916=CARTESIAN_POINT('Ctrl Pts',(-19.567233979836,25.9318020855621,10.9002001749145));
#10917=CARTESIAN_POINT('Ctrl Pts',(-19.888991263646,24.8711144190662,10.6189501749145));
#10918=CARTESIAN_POINT('Ctrl Pts',(-19.1858175508758,24.0143075901023,10.3377001749145));
#10919=CARTESIAN_POINT('Ctrl Pts',(-18.0827522448775,24.1229364083568,10.0564501749145));
#10920=CARTESIAN_POINT('Ctrl Pts',(-17.5602315759329,25.1004979111444,9.77520017491453));
#10921=CARTESIAN_POINT('Ctrl Pts',(-18.0827715699962,26.0779704411713,9.49395017491453));
#10922=CARTESIAN_POINT('Ctrl Pts',(-19.1857689049176,26.1867342513203,9.21270017491453));
#10923=CARTESIAN_POINT('Ctrl Pts',(-19.8890943967093,25.3296765835496,8.93145017491453));
#10924=CARTESIAN_POINT('Ctrl Pts',(-19.5670229443132,24.2694854426487,8.65020017491453));
#10925=CARTESIAN_POINT('Ctrl Pts',(-18.5069804208413,23.9467315923973,8.36895017491453));
#10926=CARTESIAN_POINT('Ctrl Pts',(-17.6488545534444,24.6519424250744,8.08770017491453));
#10927=CARTESIAN_POINT('Ctrl Pts',(-17.741956130451,25.5673943129456,7.85332517491453));
#10928=CARTESIAN_POINT('Ctrl Pts',(-18.2463209906547,26.0179660342054,7.66582517491453));
#10929=CARTESIAN_POINT('Ctrl Pts',(-18.5723902429877,26.1004782148047,7.57207517491453));
#10930=CARTESIAN_POINT('Ctrl Pts',(-18.7359120418715,26.1004782148047,7.52520017491453));
#10931=CARTESIAN_POINT('Ctrl Pts',(-18.7359120418715,26.1719704380264,16.3763120970567));
#10932=CARTESIAN_POINT('Ctrl Pts',(-18.9112832567962,26.1719704380264,16.3294370970567));
#10933=CARTESIAN_POINT('Ctrl Pts',(-19.2604928816873,26.0836104084264,16.2356870970568));
#10934=CARTESIAN_POINT('Ctrl Pts',(-19.8011898254895,25.6006632552387,16.0481870970567));
#10935=CARTESIAN_POINT('Ctrl Pts',(-19.9006761814027,24.6199119837374,15.8138120970568));
#10936=CARTESIAN_POINT('Ctrl Pts',(-18.9812730600262,23.8641250484612,15.5325620970567));
#10937=CARTESIAN_POINT('Ctrl Pts',(-17.8452974226091,24.2100292982365,15.2513120970568));
#10938=CARTESIAN_POINT('Ctrl Pts',(-17.5002088862725,25.3460716478709,14.9700620970567));
#10939=CARTESIAN_POINT('Ctrl Pts',(-18.2538540872815,26.2644803214233,14.6888120970568));
#10940=CARTESIAN_POINT('Ctrl Pts',(-19.4357996089,26.1479262471745,14.4075620970567));
#10941=CARTESIAN_POINT('Ctrl Pts',(-19.9957331087188,25.1005003313284,14.1263120970567));
#10942=CARTESIAN_POINT('Ctrl Pts',(-19.4358182926448,24.0529745102095,13.8450620970567));
#10943=CARTESIAN_POINT('Ctrl Pts',(-18.2538070558221,23.9365720149762,13.5638120970568));
#10944=CARTESIAN_POINT('Ctrl Pts',(-17.5003085963596,24.8546990276559,13.2825620970567));
#10945=CARTESIAN_POINT('Ctrl Pts',(-17.8450933927673,25.9912989167809,13.0013120970568));
#10946=CARTESIAN_POINT('Ctrl Pts',(-18.9816881993013,26.3360795225021,12.7200620970567));
#10947=CARTESIAN_POINT('Ctrl Pts',(-19.899823815302,25.5825865293351,12.4388120970567));
#10948=CARTESIAN_POINT('Ctrl Pts',(-19.7834047461942,24.4005657233216,12.1575620970567));
#10949=CARTESIAN_POINT('Ctrl Pts',(-18.7359120418715,23.8406695287272,11.8763120970567));
#10950=CARTESIAN_POINT('Ctrl Pts',(-17.6884193375488,24.4005657233217,11.5950620970567));
#10951=CARTESIAN_POINT('Ctrl Pts',(-17.5720002684409,25.582586529335,11.3138120970567));
#10952=CARTESIAN_POINT('Ctrl Pts',(-18.4901358844417,26.3360795225021,11.0325620970568));
#10953=CARTESIAN_POINT('Ctrl Pts',(-19.6267306909757,25.9912989167809,10.7513120970567));
#10954=CARTESIAN_POINT('Ctrl Pts',(-19.9715154873835,24.8546990276559,10.4700620970567));
#10955=CARTESIAN_POINT('Ctrl Pts',(-19.2180170279209,23.9365720149762,10.1888120970567));
#10956=CARTESIAN_POINT('Ctrl Pts',(-18.0360057910981,24.0529745102095,9.90756209705675));
#10957=CARTESIAN_POINT('Ctrl Pts',(-17.4760909750243,25.1005003313284,9.62631209705675));
#10958=CARTESIAN_POINT('Ctrl Pts',(-18.036024474843,26.1479262471745,9.34506209705674));
#10959=CARTESIAN_POINT('Ctrl Pts',(-19.2179699964615,26.2644803214233,9.06381209705675));
#10960=CARTESIAN_POINT('Ctrl Pts',(-19.9716151974705,25.3460716478709,8.78256209705674));
#10961=CARTESIAN_POINT('Ctrl Pts',(-19.6265266611339,24.2100292982365,8.50131209705674));
#10962=CARTESIAN_POINT('Ctrl Pts',(-18.4905510237168,23.8641250484612,8.22006209705674));
#10963=CARTESIAN_POINT('Ctrl Pts',(-17.5711479023404,24.6199119837374,7.93881209705675));
#10964=CARTESIAN_POINT('Ctrl Pts',(-17.6706342582534,25.6006632552387,7.70443709705674));
#10965=CARTESIAN_POINT('Ctrl Pts',(-18.2113312020557,26.0836104084263,7.51693709705675));
#10966=CARTESIAN_POINT('Ctrl Pts',(-18.5605408269468,26.1719704380264,7.42318709705674));
#10967=CARTESIAN_POINT('Ctrl Pts',(-18.7359120418715,26.1719704380264,7.37631209705674));
#10968=CARTESIAN_POINT('Ctrl Pts',(-18.7359120418715,26.4141284002705,16.3210712807239));
#10969=CARTESIAN_POINT('Ctrl Pts',(-18.9508421867125,26.4141284002705,16.2741962807239));
#10970=CARTESIAN_POINT('Ctrl Pts',(-19.3790542523568,26.305774781696,16.1804462807239));
#10971=CARTESIAN_POINT('Ctrl Pts',(-20.0418196213741,25.7137583047068,15.9929462807239));
#10972=CARTESIAN_POINT('Ctrl Pts',(-20.1639181514686,24.5112865006198,15.7585712807239));
#10973=CARTESIAN_POINT('Ctrl Pts',(-19.0366952474877,23.5847663556869,15.4773212807239));
#10974=CARTESIAN_POINT('Ctrl Pts',(-17.6440584440828,24.008809278139,15.1960712807239));
#10975=CARTESIAN_POINT('Ctrl Pts',(-17.220975640258,25.401571598331,14.9148212807239));
#10976=CARTESIAN_POINT('Ctrl Pts',(-18.1449274857128,26.5275043655938,14.6335712807239));
#10977=CARTESIAN_POINT('Ctrl Pts',(-19.5939497971795,26.3846158434426,14.3523212807239));
#10978=CARTESIAN_POINT('Ctrl Pts',(-20.2804116503335,25.1005048514074,14.0710712807239));
#10979=CARTESIAN_POINT('Ctrl Pts',(-19.5939736594703,23.8162735358942,13.7898212807239));
#10980=CARTESIAN_POINT('Ctrl Pts',(-18.1448674186095,23.6735675718114,13.5085712807239));
#10981=CARTESIAN_POINT('Ctrl Pts',(-17.2211029869125,24.7991611137086,13.2273212807239));
#10982=CARTESIAN_POINT('Ctrl Pts',(-17.6437978626977,26.1925949193548,12.9460712807239));
#10983=CARTESIAN_POINT('Ctrl Pts',(-19.0372254681633,26.6152845876365,12.6648212807239));
#10984=CARTESIAN_POINT('Ctrl Pts',(-20.1628294097853,25.6915270641991,12.3835712807239));
#10985=CARTESIAN_POINT('Ctrl Pts',(-20.0201034674711,24.2424086412214,12.1023212807239));
#10986=CARTESIAN_POINT('Ctrl Pts',(-18.7359120418715,23.5559944071884,11.8210712807239));
#10987=CARTESIAN_POINT('Ctrl Pts',(-17.451720616272,24.2424086412214,11.5398212807239));
#10988=CARTESIAN_POINT('Ctrl Pts',(-17.3089946739576,25.6915270641991,11.2585712807239));
#10989=CARTESIAN_POINT('Ctrl Pts',(-18.4345986155797,26.6152845876365,10.9773212807239));
#10990=CARTESIAN_POINT('Ctrl Pts',(-19.8280262210453,26.1925949193548,10.6960712807239));
#10991=CARTESIAN_POINT('Ctrl Pts',(-20.2507210968305,24.7991611137086,10.4148212807239));
#10992=CARTESIAN_POINT('Ctrl Pts',(-19.3269566651335,23.6735675718114,10.1335712807239));
#10993=CARTESIAN_POINT('Ctrl Pts',(-17.8778504242727,23.8162735358942,9.8523212807239));
#10994=CARTESIAN_POINT('Ctrl Pts',(-17.1914124334094,25.1005048514074,9.5710712807239));
#10995=CARTESIAN_POINT('Ctrl Pts',(-17.8778742865635,26.3846158434426,9.28982128072389));
#10996=CARTESIAN_POINT('Ctrl Pts',(-19.3268965980302,26.5275043655938,9.00857128072391));
#10997=CARTESIAN_POINT('Ctrl Pts',(-20.250848443485,25.401571598331,8.72732128072388));
#10998=CARTESIAN_POINT('Ctrl Pts',(-19.8277656396602,24.008809278139,8.44607128072391));
#10999=CARTESIAN_POINT('Ctrl Pts',(-18.4351288362553,23.5847663556869,8.16482128072388));
#11000=CARTESIAN_POINT('Ctrl Pts',(-17.3079059322744,24.5112865006198,7.88357128072391));
#11001=CARTESIAN_POINT('Ctrl Pts',(-17.4300044623689,25.7137583047068,7.6491962807239));
#11002=CARTESIAN_POINT('Ctrl Pts',(-18.0927698313862,26.305774781696,7.4616962807239));
#11003=CARTESIAN_POINT('Ctrl Pts',(-18.5209818970305,26.4141284002705,7.3679462807239));
#11004=CARTESIAN_POINT('Ctrl Pts',(-18.7359120418715,26.4141284002705,7.3210712807239));
#11005=CARTESIAN_POINT('Ctrl Pts',(-18.7359120418715,26.6084571633498,16.4758041204314));
#11006=CARTESIAN_POINT('Ctrl Pts',(-18.9826469033796,26.6084571633498,16.4289291204314));
#11007=CARTESIAN_POINT('Ctrl Pts',(-19.4741937528585,26.4840779780848,16.3351791204314));
#11008=CARTESIAN_POINT('Ctrl Pts',(-20.2350195258441,25.8044739987892,16.1476791204314));
#11009=CARTESIAN_POINT('Ctrl Pts',(-20.375163029678,24.4241294443889,15.9133041204314));
#11010=CARTESIAN_POINT('Ctrl Pts',(-19.0811941654188,23.3605387996255,15.6320541204314));
#11011=CARTESIAN_POINT('Ctrl Pts',(-17.4825347251303,23.8473153437877,15.3508041204314));
#11012=CARTESIAN_POINT('Ctrl Pts',(-16.9968656612976,25.4461130330323,15.0695541204314));
#11013=CARTESIAN_POINT('Ctrl Pts',(-18.0575004077785,26.7386103777278,14.7883041204314));
#11014=CARTESIAN_POINT('Ctrl Pts',(-19.7208829623709,26.5745833887618,14.5070541204314));
#11015=CARTESIAN_POINT('Ctrl Pts',(-20.5088956419845,25.1005088555967,14.2258041204314));
#11016=CARTESIAN_POINT('Ctrl Pts',(-19.7209102270372,23.6262959111371,13.9445541204314));
#11017=CARTESIAN_POINT('Ctrl Pts',(-18.0574317760813,23.4624789235696,13.6633041204314));
#11018=CARTESIAN_POINT('Ctrl Pts',(-16.9970111655101,24.7545860482947,13.3820541204314));
#11019=CARTESIAN_POINT('Ctrl Pts',(-17.4822369891815,26.3541561653093,13.1008041204314));
#11020=CARTESIAN_POINT('Ctrl Pts',(-19.0817999846728,26.8393760204334,12.8195541204314));
#11021=CARTESIAN_POINT('Ctrl Pts',(-20.3739190673027,25.778963312495,12.5383041204314));
#11022=CARTESIAN_POINT('Ctrl Pts',(-20.2100791005622,24.1154709374084,12.2570541204314));
#11023=CARTESIAN_POINT('Ctrl Pts',(-18.7359120418715,23.3275126699529,11.9758041204314));
#11024=CARTESIAN_POINT('Ctrl Pts',(-17.2617449831808,24.1154709374084,11.6945541204314));
#11025=CARTESIAN_POINT('Ctrl Pts',(-17.0979050164403,25.778963312495,11.4133041204314));
#11026=CARTESIAN_POINT('Ctrl Pts',(-18.3900240990702,26.8393760204334,11.1320541204314));
#11027=CARTESIAN_POINT('Ctrl Pts',(-19.9895870945615,26.3541561653093,10.8508041204314));
#11028=CARTESIAN_POINT('Ctrl Pts',(-20.4748129182329,24.7545860482946,10.5695541204314));
#11029=CARTESIAN_POINT('Ctrl Pts',(-19.4143923076617,23.4624789235696,10.2883041204314));
#11030=CARTESIAN_POINT('Ctrl Pts',(-17.7509138567058,23.6262959111371,10.0070541204314));
#11031=CARTESIAN_POINT('Ctrl Pts',(-16.9629284417585,25.1005088555967,9.72580412043144));
#11032=CARTESIAN_POINT('Ctrl Pts',(-17.7509411213721,26.5745833887619,9.44455412043143));
#11033=CARTESIAN_POINT('Ctrl Pts',(-19.4143236759645,26.7386103777278,9.16330412043143));
#11034=CARTESIAN_POINT('Ctrl Pts',(-20.4749584224454,25.4461130330323,8.88205412043143));
#11035=CARTESIAN_POINT('Ctrl Pts',(-19.9892893586127,23.8473153437877,8.60080412043143));
#11036=CARTESIAN_POINT('Ctrl Pts',(-18.3906299183242,23.3605387996255,8.31955412043143));
#11037=CARTESIAN_POINT('Ctrl Pts',(-17.096661054065,24.4241294443889,8.03830412043144));
#11038=CARTESIAN_POINT('Ctrl Pts',(-17.2368045578989,25.8044739987892,7.80392912043142));
#11039=CARTESIAN_POINT('Ctrl Pts',(-17.9976303308845,26.4840779780847,7.61642912043144));
#11040=CARTESIAN_POINT('Ctrl Pts',(-18.4891771803634,26.6084571633498,7.52267912043143));
#11041=CARTESIAN_POINT('Ctrl Pts',(-18.7359120418715,26.6084571633498,7.47580412043143));
#11042=CARTESIAN_POINT('Ctrl Pts',(-18.7359120418715,26.6081737492155,16.7240897479859));
#11043=CARTESIAN_POINT('Ctrl Pts',(-18.9826173818796,26.6081737492155,16.6772147479859));
#11044=CARTESIAN_POINT('Ctrl Pts',(-19.4740537078383,26.4838233629858,16.5834647479859));
#11045=CARTESIAN_POINT('Ctrl Pts',(-20.2347655405055,25.8043298167281,16.3959647479859));
#11046=CARTESIAN_POINT('Ctrl Pts',(-20.3748539357312,24.4242604178057,16.1615897479859));
#11047=CARTESIAN_POINT('Ctrl Pts',(-19.0811359078137,23.360852802763,15.8803397479859));
#11048=CARTESIAN_POINT('Ctrl Pts',(-17.4827611940112,23.8475459221466,15.5990897479859));
#11049=CARTESIAN_POINT('Ctrl Pts',(-16.9971843119434,25.4460490452383,15.3178397479859));
#11050=CARTESIAN_POINT('Ctrl Pts',(-18.0576236867847,26.7383117517441,15.0365897479859));
#11051=CARTESIAN_POINT('Ctrl Pts',(-19.7207034259278,26.574314052913,14.7553397479859));
#11052=CARTESIAN_POINT('Ctrl Pts',(-20.5085718179255,25.1005089571751,14.4740897479859));
#11053=CARTESIAN_POINT('Ctrl Pts',(-19.7207304709154,23.6265649912903,14.1928397479859));
#11054=CARTESIAN_POINT('Ctrl Pts',(-18.0575556080725,23.4627779900428,13.9115897479859));
#11055=CARTESIAN_POINT('Ctrl Pts',(-16.9973286437738,24.7546491829152,13.6303397479859));
#11056=CARTESIAN_POINT('Ctrl Pts',(-17.4824658571953,26.3539272948311,13.3490897479859));
#11057=CARTESIAN_POINT('Ctrl Pts',(-19.0817368419513,26.8390585564741,13.0678397479859));
#11058=CARTESIAN_POINT('Ctrl Pts',(-20.3736200236858,25.778839446961,12.7865897479859));
#11059=CARTESIAN_POINT('Ctrl Pts',(-20.2098099709757,24.1156507636605,12.5053397479859));
#11060=CARTESIAN_POINT('Ctrl Pts',(-18.7359120418715,23.3278363510213,12.2240897479859));
#11061=CARTESIAN_POINT('Ctrl Pts',(-17.2620141127673,24.1156507636606,11.9428397479859));
#11062=CARTESIAN_POINT('Ctrl Pts',(-17.0982040600572,25.778839446961,11.6615897479859));
#11063=CARTESIAN_POINT('Ctrl Pts',(-18.3900872417917,26.8390585564741,11.3803397479859));
#11064=CARTESIAN_POINT('Ctrl Pts',(-19.9893582265476,26.3539272948311,11.0990897479859));
#11065=CARTESIAN_POINT('Ctrl Pts',(-20.4744954399692,24.7546491829153,10.8178397479859));
#11066=CARTESIAN_POINT('Ctrl Pts',(-19.4142684756705,23.4627779900428,10.5365897479859));
#11067=CARTESIAN_POINT('Ctrl Pts',(-17.7510936128276,23.6265649912903,10.2553397479859));
#11068=CARTESIAN_POINT('Ctrl Pts',(-16.9632522658175,25.1005089571751,9.97408974798591));
#11069=CARTESIAN_POINT('Ctrl Pts',(-17.7511206578151,26.574314052913,9.69283974798589));
#11070=CARTESIAN_POINT('Ctrl Pts',(-19.4142003969583,26.7383117517442,9.41158974798592));
#11071=CARTESIAN_POINT('Ctrl Pts',(-20.4746397717996,25.4460490452383,9.1303397479859));
#11072=CARTESIAN_POINT('Ctrl Pts',(-19.9890628897318,23.8475459221467,8.84908974798591));
#11073=CARTESIAN_POINT('Ctrl Pts',(-18.3906881759293,23.360852802763,8.5678397479859));
#11074=CARTESIAN_POINT('Ctrl Pts',(-17.0969701480118,24.4242604178057,8.2865897479859));
#11075=CARTESIAN_POINT('Ctrl Pts',(-17.2370585432375,25.804329816728,8.05221474798591));
#11076=CARTESIAN_POINT('Ctrl Pts',(-17.9977703759046,26.4838233629858,7.8647147479859));
#11077=CARTESIAN_POINT('Ctrl Pts',(-18.4892067018634,26.6081737492155,7.7709647479859));
#11078=CARTESIAN_POINT('Ctrl Pts',(-18.7359120418715,26.6081737492155,7.7240897479859));
#11079=CARTESIAN_POINT('Ctrl Pts',(-18.7359120418715,26.4142031825479,16.8791537727106));
#11080=CARTESIAN_POINT('Ctrl Pts',(-18.9508538798108,26.4142031825479,16.8322787727106));
#11081=CARTESIAN_POINT('Ctrl Pts',(-19.3790909060845,26.305843221212,16.7385287727106));
#11082=CARTESIAN_POINT('Ctrl Pts',(-20.0418930695294,25.7137935989603,16.5510287727106));
#11083=CARTESIAN_POINT('Ctrl Pts',(-20.1639994761375,24.5112528354905,16.3166537727106));
#11084=CARTESIAN_POINT('Ctrl Pts',(-19.0367121566617,23.5846804891688,16.0354037727106));
#11085=CARTESIAN_POINT('Ctrl Pts',(-17.6439965807029,24.0087472917322,15.7541537727107));
#11086=CARTESIAN_POINT('Ctrl Pts',(-17.2208896629275,25.4015887074258,15.4729037727106));
#11087=CARTESIAN_POINT('Ctrl Pts',(-18.1448939786028,26.5275853043863,15.1916537727106));
#11088=CARTESIAN_POINT('Ctrl Pts',(-19.5939984631419,26.3846886974873,14.9104037727106));
#11089=CARTESIAN_POINT('Ctrl Pts',(-20.2804992718394,25.1005048494697,14.6291537727106));
#11090=CARTESIAN_POINT('Ctrl Pts',(-19.5940223336954,23.8162006867272,14.3479037727106));
#11091=CARTESIAN_POINT('Ctrl Pts',(-18.1448338907002,23.673486624616,14.0666537727106));
#11092=CARTESIAN_POINT('Ctrl Pts',(-17.2210170536785,24.7991440208896,13.7854037727106));
#11093=CARTESIAN_POINT('Ctrl Pts',(-17.6437359090807,26.1926568731773,13.5041537727106));
#11094=CARTESIAN_POINT('Ctrl Pts',(-19.0372425610592,26.615370520276,13.2229037727106));
#11095=CARTESIAN_POINT('Ctrl Pts',(-20.1629103565813,25.6915605933992,12.9416537727106));
#11096=CARTESIAN_POINT('Ctrl Pts',(-20.0201763175665,24.2423599643414,12.6604037727107));
#11097=CARTESIAN_POINT('Ctrl Pts',(-18.7359120418715,23.5559067910743,12.3791537727106));
#11098=CARTESIAN_POINT('Ctrl Pts',(-17.4516477661765,24.2423599643414,12.0979037727106));
#11099=CARTESIAN_POINT('Ctrl Pts',(-17.3089137271617,25.6915605933992,11.8166537727106));
#11100=CARTESIAN_POINT('Ctrl Pts',(-18.4345815226838,26.615370520276,11.5354037727106));
#11101=CARTESIAN_POINT('Ctrl Pts',(-19.8280881746623,26.1926568731773,11.2541537727106));
#11102=CARTESIAN_POINT('Ctrl Pts',(-20.2508070300645,24.7991440208897,10.9729037727106));
#11103=CARTESIAN_POINT('Ctrl Pts',(-19.3269901930428,23.673486624616,10.6916537727106));
#11104=CARTESIAN_POINT('Ctrl Pts',(-17.8778017500476,23.8162006867272,10.4104037727106));
#11105=CARTESIAN_POINT('Ctrl Pts',(-17.1913248119037,25.1005048494697,10.1291537727106));
#11106=CARTESIAN_POINT('Ctrl Pts',(-17.8778256206011,26.3846886974873,9.84790377271063));
#11107=CARTESIAN_POINT('Ctrl Pts',(-19.3269301051402,26.5275853043863,9.56665377271064));
#11108=CARTESIAN_POINT('Ctrl Pts',(-20.2509344208154,25.4015887074258,9.28540377271063));
#11109=CARTESIAN_POINT('Ctrl Pts',(-19.8278275030402,24.0087472917322,9.00415377271064));
#11110=CARTESIAN_POINT('Ctrl Pts',(-18.4351119270813,23.5846804891688,8.72290377271064));
#11111=CARTESIAN_POINT('Ctrl Pts',(-17.3078246076055,24.5112528354905,8.44165377271065));
#11112=CARTESIAN_POINT('Ctrl Pts',(-17.4299310142136,25.7137935989603,8.20727877271063));
#11113=CARTESIAN_POINT('Ctrl Pts',(-18.0927331776585,26.3058432212119,8.01977877271064));
#11114=CARTESIAN_POINT('Ctrl Pts',(-18.5209702039323,26.4142031825479,7.92602877271064));
#11115=CARTESIAN_POINT('Ctrl Pts',(-18.7359120418715,26.4142031825479,7.87915377271064));
#11116=CARTESIAN_POINT('Ctrl Pts',(-18.7359120418715,26.1720057758739,16.8236417604652));
#11117=CARTESIAN_POINT('Ctrl Pts',(-18.9112831752672,26.1720057758739,16.7767667604652));
#11118=CARTESIAN_POINT('Ctrl Pts',(-19.2605106314382,26.0836409446025,16.6830167604652));
#11119=CARTESIAN_POINT('Ctrl Pts',(-19.8012152953036,25.6006838833452,16.4955167604651));
#11120=CARTESIAN_POINT('Ctrl Pts',(-19.9007149462722,24.6198947916415,16.2611417604652));
#11121=CARTESIAN_POINT('Ctrl Pts',(-18.9812788422948,23.8640888006839,15.9798917604651));
#11122=CARTESIAN_POINT('Ctrl Pts',(-17.8452712157343,24.21000165239,15.6986417604652));
#11123=CARTESIAN_POINT('Ctrl Pts',(-17.5001709838288,25.3460794092692,15.4173917604651));
#11124=CARTESIAN_POINT('Ctrl Pts',(-18.2538396591719,26.264515490713,15.1361417604652));
#11125=CARTESIAN_POINT('Ctrl Pts',(-19.4358207482657,26.1479581077059,14.8548917604651));
#11126=CARTESIAN_POINT('Ctrl Pts',(-19.995771387193,25.1005002946964,14.5736417604652));
#11127=CARTESIAN_POINT('Ctrl Pts',(-19.4358395073079,24.052942741889,14.2923917604651));
#11128=CARTESIAN_POINT('Ctrl Pts',(-18.2537924381707,23.9365366868337,14.0111417604652));
#11129=CARTESIAN_POINT('Ctrl Pts',(-17.500271095763,24.8546915739354,13.7298917604652));
#11130=CARTESIAN_POINT('Ctrl Pts',(-17.8450663635619,25.9913259467221,13.4486417604652));
#11131=CARTESIAN_POINT('Ctrl Pts',(-18.981695656018,26.3361170182501,13.1673917604652));
#11132=CARTESIAN_POINT('Ctrl Pts',(-19.8998591351667,25.5826011584555,12.8861417604651));
#11133=CARTESIAN_POINT('Ctrl Pts',(-19.7834365323557,24.400544484637,12.6048917604652));
#11134=CARTESIAN_POINT('Ctrl Pts',(-18.7359120418715,23.8406312992516,12.3236417604652));
#11135=CARTESIAN_POINT('Ctrl Pts',(-17.6883875513873,24.400544484637,12.0423917604652));
#11136=CARTESIAN_POINT('Ctrl Pts',(-17.5719649485763,25.5826011584555,11.7611417604651));
#11137=CARTESIAN_POINT('Ctrl Pts',(-18.490128427725,26.3361170182501,11.4798917604652));
#11138=CARTESIAN_POINT('Ctrl Pts',(-19.6267577201811,25.9913259467221,11.1986417604651));
#11139=CARTESIAN_POINT('Ctrl Pts',(-19.97155298798,24.8546915739354,10.9173917604652));
#11140=CARTESIAN_POINT('Ctrl Pts',(-19.2180316455722,23.9365366868336,10.6361417604652));
#11141=CARTESIAN_POINT('Ctrl Pts',(-18.0359845764351,24.052942741889,10.3548917604651));
#11142=CARTESIAN_POINT('Ctrl Pts',(-17.4760526965499,25.1005002946963,10.0736417604652));
#11143=CARTESIAN_POINT('Ctrl Pts',(-18.0360033354773,26.1479581077059,9.79239176046515));
#11144=CARTESIAN_POINT('Ctrl Pts',(-19.217984424571,26.264515490713,9.51114176046517));
#11145=CARTESIAN_POINT('Ctrl Pts',(-19.9716530999141,25.3460794092692,9.22989176046515));
#11146=CARTESIAN_POINT('Ctrl Pts',(-19.6265528680087,24.21000165239,8.94864176046517));
#11147=CARTESIAN_POINT('Ctrl Pts',(-18.4905452414482,23.8640888006839,8.66739176046515));
#11148=CARTESIAN_POINT('Ctrl Pts',(-17.5711091374708,24.6198947916415,8.38614176046516));
#11149=CARTESIAN_POINT('Ctrl Pts',(-17.6706087884394,25.6006838833452,8.15176676046515));
#11150=CARTESIAN_POINT('Ctrl Pts',(-18.2113134523048,26.0836409446025,7.96426676046516));
#11151=CARTESIAN_POINT('Ctrl Pts',(-18.5605409084758,26.1720057758739,7.87051676046516));
#11152=CARTESIAN_POINT('Ctrl Pts',(-18.7359120418715,26.1720057758739,7.82364176046516));
#11153=CARTESIAN_POINT('Ctrl Pts',(-18.7359120418715,26.1004782148047,16.6747998250855));
#11154=CARTESIAN_POINT('Ctrl Pts',(-18.8994244050499,26.1004782148047,16.6279248250855));
#11155=CARTESIAN_POINT('Ctrl Pts',(-19.225503815506,26.0179629976208,16.5341748250855));
#11156=CARTESIAN_POINT('Ctrl Pts',(-19.729852407908,25.5674009602397,16.3466748250855));
#11157=CARTESIAN_POINT('Ctrl Pts',(-19.8229700948236,24.6519402645263,16.1122998250855));
#11158=CARTESIAN_POINT('Ctrl Pts',(-18.9648399471218,23.9467388754675,15.8310498250855));
#11159=CARTESIAN_POINT('Ctrl Pts',(-17.9048062320946,24.2694882115908,15.5497998250855));
#11160=CARTESIAN_POINT('Ctrl Pts',(-17.5827342736889,25.3296760393435,15.2685498250855));
#11161=CARTESIAN_POINT('Ctrl Pts',(-18.2860575439579,26.1867290719232,14.9872998250855));
#11162=CARTESIAN_POINT('Ctrl Pts',(-19.389049388048,26.0779661227699,14.7060498250855));
#11163=CARTESIAN_POINT('Ctrl Pts',(-19.9115872464834,25.1004978510395,14.4247998250855));
#11164=CARTESIAN_POINT('Ctrl Pts',(-19.3890688333093,24.1229408780555,14.1435498250855));
#11165=CARTESIAN_POINT('Ctrl Pts',(-18.2860085955716,24.0143125088581,13.8622998250855));
#11166=CARTESIAN_POINT('Ctrl Pts',(-17.5828380479293,24.8711154681011,13.5810498250855));
#11167=CARTESIAN_POINT('Ctrl Pts',(-17.904593884481,25.931798306063,13.2997998250855));
#11168=CARTESIAN_POINT('Ctrl Pts',(-18.9652720442565,26.2535500850915,13.0185498250855));
#11169=CARTESIAN_POINT('Ctrl Pts',(-19.8220827220082,25.5503850729478,12.7372998250855));
#11170=CARTESIAN_POINT('Ctrl Pts',(-19.7134396018004,24.4473149586569,12.4560498250855));
#11171=CARTESIAN_POINT('Ctrl Pts',(-18.7359120418715,23.9248158714588,12.1747998250854));
#11172=CARTESIAN_POINT('Ctrl Pts',(-17.7583844819426,24.4473149586569,11.8935498250855));
#11173=CARTESIAN_POINT('Ctrl Pts',(-17.6497413617348,25.5503850729478,11.6122998250855));
#11174=CARTESIAN_POINT('Ctrl Pts',(-18.5065520394865,26.2535500850916,11.3310498250855));
#11175=CARTESIAN_POINT('Ctrl Pts',(-19.5672301992619,25.931798306063,11.0497998250855));
#11176=CARTESIAN_POINT('Ctrl Pts',(-19.8889860358136,24.8711154681011,10.7685498250855));
#11177=CARTESIAN_POINT('Ctrl Pts',(-19.1858154881714,24.0143125088581,10.4872998250855));
#11178=CARTESIAN_POINT('Ctrl Pts',(-18.0827552504337,24.1229408780555,10.2060498250855));
#11179=CARTESIAN_POINT('Ctrl Pts',(-17.5602368372596,25.1004978510396,9.92479982508548));
#11180=CARTESIAN_POINT('Ctrl Pts',(-18.0827746956949,26.0779661227699,9.64354982508546));
#11181=CARTESIAN_POINT('Ctrl Pts',(-19.1857665397851,26.1867290719232,9.36229982508548));
#11182=CARTESIAN_POINT('Ctrl Pts',(-19.8890898100541,25.3296760393435,9.08104982508546));
#11183=CARTESIAN_POINT('Ctrl Pts',(-19.5670178516484,24.2694882115909,8.79979982508548));
#11184=CARTESIAN_POINT('Ctrl Pts',(-18.5069841366212,23.9467388754675,8.51854982508546));
#11185=CARTESIAN_POINT('Ctrl Pts',(-17.6488539889194,24.6519402645264,8.23729982508548));
#11186=CARTESIAN_POINT('Ctrl Pts',(-17.741971675835,25.5674009602396,8.00292482508546));
#11187=CARTESIAN_POINT('Ctrl Pts',(-18.246320268237,26.0179629976208,7.81542482508548));
#11188=CARTESIAN_POINT('Ctrl Pts',(-18.5723996786931,26.1004782148047,7.72167482508547));
#11189=CARTESIAN_POINT('Ctrl Pts',(-18.7359120418715,26.1004782148047,7.67479982508547));
#11190=CARTESIAN_POINT('Ctrl Pts',(-18.7359120418715,26.1004782148047,16.6));
#11191=CARTESIAN_POINT('Ctrl Pts',(-18.899536659246,26.1004782148047,16.553125));
#11192=CARTESIAN_POINT('Ctrl Pts',(-19.2254952210856,26.0179991230989,16.459375));
#11193=CARTESIAN_POINT('Ctrl Pts',(-19.7300373474021,25.5673218790664,16.271875));
#11194=CARTESIAN_POINT('Ctrl Pts',(-19.8229633788124,24.6519659680192,16.0375));
#11195=CARTESIAN_POINT('Ctrl Pts',(-18.9648841528132,23.9466522306267,15.75625));
#11196=CARTESIAN_POINT('Ctrl Pts',(-17.9047456459512,24.2694552701876,15.475));
#11197=CARTESIAN_POINT('Ctrl Pts',(-17.5826797074142,25.3296825136249,15.19375));
#11198=CARTESIAN_POINT('Ctrl Pts',(-18.2860294065758,26.1867906898977,14.9125));
#11199=CARTESIAN_POINT('Ctrl Pts',(-19.389086573694,26.0780174976981,14.63125));
#11200=CARTESIAN_POINT('Ctrl Pts',(-19.9116498391532,25.1004985660911,14.35));
#11201=CARTESIAN_POINT('Ctrl Pts',(-19.3891045896494,24.1228877031823,14.06875));
#11202=CARTESIAN_POINT('Ctrl Pts',(-18.2859840561,24.0142539916667,13.7875));
#11203=CARTESIAN_POINT('Ctrl Pts',(-17.582775853732,24.8711029879984,13.50625));
#11204=CARTESIAN_POINT('Ctrl Pts',(-17.9045489079489,25.9318432698064,13.225));
#11205=CARTESIAN_POINT('Ctrl Pts',(-18.9652844651045,26.2536123707356,12.94375));
#11206=CARTESIAN_POINT('Ctrl Pts',(-19.8221414011456,25.5504093950162,12.6625));
#11207=CARTESIAN_POINT('Ctrl Pts',(-19.7134924282747,24.4472796581219,12.38125));
#11208=CARTESIAN_POINT('Ctrl Pts',(-18.7359120418715,23.9247523488297,12.1));
#11209=CARTESIAN_POINT('Ctrl Pts',(-17.7583316554683,24.4472796581219,11.81875));
#11210=CARTESIAN_POINT('Ctrl Pts',(-17.6496826825974,25.5504093950162,11.5375));
#11211=CARTESIAN_POINT('Ctrl Pts',(-18.5065396186384,26.2536123707357,11.25625));
#11212=CARTESIAN_POINT('Ctrl Pts',(-19.567275175794,25.9318432698063,10.975));
#11213=CARTESIAN_POINT('Ctrl Pts',(-19.8890482300109,24.8711029879984,10.69375));
#11214=CARTESIAN_POINT('Ctrl Pts',(-19.185840027643,24.0142539916666,10.4125));
#11215=CARTESIAN_POINT('Ctrl Pts',(-18.0827194940936,24.1228877031824,10.13125));
#11216=CARTESIAN_POINT('Ctrl Pts',(-17.5601742445898,25.1004985660911,9.85));
#11217=CARTESIAN_POINT('Ctrl Pts',(-18.082737510049,26.0780174976981,9.56875));
#11218=CARTESIAN_POINT('Ctrl Pts',(-19.1857946771672,26.1867906898977,9.2875));
#11219=CARTESIAN_POINT('Ctrl Pts',(-19.8891443763288,25.329682513625,9.00625));
#11220=CARTESIAN_POINT('Ctrl Pts',(-19.5670784377918,24.2694552701875,8.725));
#11221=CARTESIAN_POINT('Ctrl Pts',(-18.5069399309298,23.9466522306267,8.44375));
#11222=CARTESIAN_POINT('Ctrl Pts',(-17.6488607049306,24.6519659680192,8.16250000000001));
#11223=CARTESIAN_POINT('Ctrl Pts',(-17.7417867363409,25.5673218790663,7.928125));
#11224=CARTESIAN_POINT('Ctrl Pts',(-18.2463288626574,26.0179991230989,7.740625));
#11225=CARTESIAN_POINT('Ctrl Pts',(-18.572287424497,26.1004782148047,7.646875));
#11226=CARTESIAN_POINT('Ctrl Pts',(-18.7359120418715,26.1004782148047,7.6));
#11227=CARTESIAN_POINT('',(-18.7359120418715,26.1004782148047,7.6));
#11228=CARTESIAN_POINT('Ctrl Pts',(-18.7359120418715,26.1004782148047,16.6));
#11229=CARTESIAN_POINT('Ctrl Pts',(-18.899536659246,26.1004782148047,16.553125));
#11230=CARTESIAN_POINT('Ctrl Pts',(-19.2254952210856,26.0179991230989,16.459375));
#11231=CARTESIAN_POINT('Ctrl Pts',(-19.7300373474021,25.5673218790664,16.271875));
#11232=CARTESIAN_POINT('Ctrl Pts',(-19.8229633788124,24.6519659680192,16.0375));
#11233=CARTESIAN_POINT('Ctrl Pts',(-18.9648841528132,23.9466522306267,15.75625));
#11234=CARTESIAN_POINT('Ctrl Pts',(-17.9047456459512,24.2694552701876,15.475));
#11235=CARTESIAN_POINT('Ctrl Pts',(-17.5826797074142,25.3296825136249,15.19375));
#11236=CARTESIAN_POINT('Ctrl Pts',(-18.2860294065758,26.1867906898977,14.9125));
#11237=CARTESIAN_POINT('Ctrl Pts',(-19.389086573694,26.0780174976981,14.63125));
#11238=CARTESIAN_POINT('Ctrl Pts',(-19.9116498391532,25.1004985660911,14.35));
#11239=CARTESIAN_POINT('Ctrl Pts',(-19.3891045896494,24.1228877031823,14.06875));
#11240=CARTESIAN_POINT('Ctrl Pts',(-18.2859840561,24.0142539916667,13.7875));
#11241=CARTESIAN_POINT('Ctrl Pts',(-17.582775853732,24.8711029879984,13.50625));
#11242=CARTESIAN_POINT('Ctrl Pts',(-17.9045489079489,25.9318432698064,13.225));
#11243=CARTESIAN_POINT('Ctrl Pts',(-18.9652844651045,26.2536123707356,12.94375));
#11244=CARTESIAN_POINT('Ctrl Pts',(-19.8221414011456,25.5504093950162,12.6625));
#11245=CARTESIAN_POINT('Ctrl Pts',(-19.7134924282747,24.4472796581219,12.38125));
#11246=CARTESIAN_POINT('Ctrl Pts',(-18.7359120418715,23.9247523488297,12.1));
#11247=CARTESIAN_POINT('Ctrl Pts',(-17.7583316554683,24.4472796581219,11.81875));
#11248=CARTESIAN_POINT('Ctrl Pts',(-17.6496826825974,25.5504093950162,11.5375));
#11249=CARTESIAN_POINT('Ctrl Pts',(-18.5065396186384,26.2536123707357,11.25625));
#11250=CARTESIAN_POINT('Ctrl Pts',(-19.567275175794,25.9318432698063,10.975));
#11251=CARTESIAN_POINT('Ctrl Pts',(-19.8890482300109,24.8711029879984,10.69375));
#11252=CARTESIAN_POINT('Ctrl Pts',(-19.185840027643,24.0142539916666,10.4125));
#11253=CARTESIAN_POINT('Ctrl Pts',(-18.0827194940936,24.1228877031824,10.13125));
#11254=CARTESIAN_POINT('Ctrl Pts',(-17.5601742445898,25.1004985660911,9.85));
#11255=CARTESIAN_POINT('Ctrl Pts',(-18.082737510049,26.0780174976981,9.56875));
#11256=CARTESIAN_POINT('Ctrl Pts',(-19.1857946771672,26.1867906898977,9.2875));
#11257=CARTESIAN_POINT('Ctrl Pts',(-19.8891443763288,25.329682513625,9.00625));
#11258=CARTESIAN_POINT('Ctrl Pts',(-19.5670784377918,24.2694552701875,8.725));
#11259=CARTESIAN_POINT('Ctrl Pts',(-18.5069399309298,23.9466522306267,8.44375));
#11260=CARTESIAN_POINT('Ctrl Pts',(-17.6488607049306,24.6519659680192,8.16250000000001));
#11261=CARTESIAN_POINT('Ctrl Pts',(-17.7417867363409,25.5673218790663,7.928125));
#11262=CARTESIAN_POINT('Ctrl Pts',(-18.2463288626574,26.0179991230989,7.740625));
#11263=CARTESIAN_POINT('Ctrl Pts',(-18.572287424497,26.1004782148047,7.646875));
#11264=CARTESIAN_POINT('Ctrl Pts',(-18.7359120418715,26.1004782148047,7.6));
#11265=CARTESIAN_POINT('Origin',(-18.7359120418715,26.3504782148047,7.6));
#11266=CARTESIAN_POINT('Origin',(-18.7359120418715,26.3504782148047,7.6));
#11367=UNCERTAINTY_MEASURE_WITH_UNIT(LENGTH_MEASURE(0.01),#11386,
'DISTANCE_ACCURACY_VALUE',
'Maximum model space distance between geometric entities at asserted c
onnectivities');
#11370=UNCERTAINTY_MEASURE_WITH_UNIT(LENGTH_MEASURE(0.01),#11386,
'DISTANCE_ACCURACY_VALUE',
'Maximum model space distance between geometric entities at asserted c
onnectivities');
#11382=(
GEOMETRIC_REPRESENTATION_CONTEXT(3)
GLOBAL_UNCERTAINTY_ASSIGNED_CONTEXT((#11367))
GLOBAL_UNIT_ASSIGNED_CONTEXT((#11386,#11388,#11389))
REPRESENTATION_CONTEXT('','3D')
);
#11385=(
GEOMETRIC_REPRESENTATION_CONTEXT(3)
GLOBAL_UNCERTAINTY_ASSIGNED_CONTEXT((#11370))
GLOBAL_UNIT_ASSIGNED_CONTEXT((#11386,#11388,#11389))
REPRESENTATION_CONTEXT('','3D')
);
#11386=(
LENGTH_UNIT()
NAMED_UNIT(*)
SI_UNIT(.MILLI.,.METRE.)
);
#11388=(
NAMED_UNIT(*)
PLANE_ANGLE_UNIT()
SI_UNIT($,.RADIAN.)
);
#11389=(
NAMED_UNIT(*)
SI_UNIT($,.STERADIAN.)
SOLID_ANGLE_UNIT()
);
#11401=SHAPE_DEFINITION_REPRESENTATION(#11415,#11442);
#11415=PRODUCT_DEFINITION_SHAPE('',$,#11457);
#11442=SHAPE_REPRESENTATION('',(#6059),#11382);
#11445=PRODUCT_DEFINITION_CONTEXT('part definition',#11489,'design');
#11457=PRODUCT_DEFINITION('Spring_03','Spring_03',#11471,#11445);
#11471=PRODUCT_DEFINITION_FORMATION('',$,#11502);
#11489=APPLICATION_CONTEXT(
'Core Data for Automotive Mechanical Design Process');
#11490=PRODUCT_CONTEXT('part definition',#11489,'mechanical');
#11502=PRODUCT('Spring_03','Spring_03',$,(#11490));
#11561=COLOUR_RGB('Grey',0.48,0.52,0.57);
#11562=FILL_AREA_STYLE_COLOUR('',#11561);
#11563=FILL_AREA_STYLE('',(#11562));
#11564=SURFACE_STYLE_FILL_AREA(#11563);
#11565=SURFACE_SIDE_STYLE('',(#11564));
#11566=SURFACE_STYLE_USAGE(.BOTH.,#11565);
#11567=PRESENTATION_STYLE_ASSIGNMENT((#11566));
ENDSEC;
END-ISO-10303-21;
